ISO-10303-21;
HEADER;
/* Generated by software containing ST-Developer
 * from STEP Tools, Inc. (www.steptools.com) 
 */

FILE_DESCRIPTION(
/* description */ ('Bell-crank linkage with push rods'),
/* implementation_level */ '2;1');

FILE_NAME(
/* name */ 'Socket Set Screw - M4x6.step',
/* time_stamp */ '2026-10-28T03:25:15-07:00',
/* author */ (''),
/* organization */ (''),
/* preprocessor_version */ 'ST-DEVELOPER v20.2',
/* originating_system */ 'Autodesk Translation Framework v15.17.0.0',
/* authorisation */ '');

FILE_SCHEMA (('AUTOMOTIVE_DESIGN { 1 0 10303 214 3 1 1 }'));
ENDSEC;

DATA;
#10=MECHANICAL_DESIGN_GEOMETRIC_PRESENTATION_REPRESENTATION('',(#628),#16678);
#441=CONICAL_SURFACE('',#9940,0.185,0.785398163397449);
#442=CONICAL_SURFACE('',#9944,0.1625,0.785398163397449);
#512=SHAPE_REPRESENTATION_RELATIONSHIP('SRR','None',#16929,#566);
#566=ADVANCED_BREP_SHAPE_REPRESENTATION('',(#689),#16634);
#628=STYLED_ITEM('',(#17298),#689);
#689=MANIFOLD_SOLID_BREP('Body1',#8819);
#822=FACE_BOUND('',#2092,.T.);
#1073=PLANE('',#9931);
#1074=PLANE('',#9932);
#1075=PLANE('',#9933);
#1076=PLANE('',#9934);
#1077=PLANE('',#9935);
#1078=PLANE('',#9936);
#1079=PLANE('',#9937);
#1080=PLANE('',#9938);
#1081=PLANE('',#9946);
#1465=FACE_OUTER_BOUND('',#2084,.T.);
#1466=FACE_OUTER_BOUND('',#2085,.T.);
#1467=FACE_OUTER_BOUND('',#2086,.T.);
#1468=FACE_OUTER_BOUND('',#2087,.T.);
#1469=FACE_OUTER_BOUND('',#2088,.T.);
#1470=FACE_OUTER_BOUND('',#2089,.T.);
#1471=FACE_OUTER_BOUND('',#2090,.T.);
#1472=FACE_OUTER_BOUND('',#2091,.T.);
#1473=FACE_OUTER_BOUND('',#2093,.T.);
#1474=FACE_OUTER_BOUND('',#2094,.T.);
#1475=FACE_OUTER_BOUND('',#2095,.T.);
#1476=FACE_OUTER_BOUND('',#2096,.T.);
#2084=EDGE_LOOP('',(#6897,#6898,#6899,#6900));
#2085=EDGE_LOOP('',(#6901,#6902,#6903,#6904));
#2086=EDGE_LOOP('',(#6905,#6906,#6907,#6908));
#2087=EDGE_LOOP('',(#6909,#6910,#6911,#6912));
#2088=EDGE_LOOP('',(#6913,#6914,#6915,#6916));
#2089=EDGE_LOOP('',(#6917,#6918,#6919,#6920));
#2090=EDGE_LOOP('',(#6921,#6922,#6923,#6924,#6925,#6926));
#2091=EDGE_LOOP('',(#6927));
#2092=EDGE_LOOP('',(#6928,#6929,#6930,#6931,#6932,#6933));
#2093=EDGE_LOOP('',(#6934,#6935,#6936,#6937));
#2094=EDGE_LOOP('',(#6938,#6939,#6940,#6941));
#2095=EDGE_LOOP('',(#6942,#6943,#6944,#6945));
#2096=EDGE_LOOP('',(#6946));
#2757=LINE('',#15078,#3306);
#2758=LINE('',#15080,#3307);
#2759=LINE('',#15082,#3308);
#2760=LINE('',#15083,#3309);
#2761=LINE('',#15086,#3310);
#2762=LINE('',#15088,#3311);
#2763=LINE('',#15089,#3312);
#2764=LINE('',#15092,#3313);
#2765=LINE('',#15094,#3314);
#2766=LINE('',#15095,#3315);
#2767=LINE('',#15098,#3316);
#2768=LINE('',#15100,#3317);
#2769=LINE('',#15101,#3318);
#2770=LINE('',#15104,#3319);
#2771=LINE('',#15106,#3320);
#2772=LINE('',#15107,#3321);
#2773=LINE('',#15109,#3322);
#2774=LINE('',#15110,#3323);
#2775=LINE('',#15118,#3324);
#2776=LINE('',#15122,#3325);
#2777=LINE('',#15126,#3326);
#3306=VECTOR('',#11811,1.);
#3307=VECTOR('',#11812,1.);
#3308=VECTOR('',#11813,1.);
#3309=VECTOR('',#11814,1.);
#3310=VECTOR('',#11817,1.);
#3311=VECTOR('',#11818,1.);
#3312=VECTOR('',#11819,1.);
#3313=VECTOR('',#11822,1.);
#3314=VECTOR('',#11823,1.);
#3315=VECTOR('',#11824,1.);
#3316=VECTOR('',#11827,1.);
#3317=VECTOR('',#11828,1.);
#3318=VECTOR('',#11829,1.);
#3319=VECTOR('',#11832,1.);
#3320=VECTOR('',#11833,1.);
#3321=VECTOR('',#11834,1.);
#3322=VECTOR('',#11837,1.);
#3323=VECTOR('',#11838,1.);
#3324=VECTOR('',#11849,0.185);
#3325=VECTOR('',#11854,0.2);
#3326=VECTOR('',#11859,0.1625);
#3864=CIRCLE('',#9939,0.17);
#3865=CIRCLE('',#9941,0.1954);
#3866=CIRCLE('',#9943,0.1954);
#3867=CIRCLE('',#9945,0.125);
#4446=VERTEX_POINT('',#15076);
#4447=VERTEX_POINT('',#15077);
#4448=VERTEX_POINT('',#15079);
#4449=VERTEX_POINT('',#15081);
#4450=VERTEX_POINT('',#15085);
#4451=VERTEX_POINT('',#15087);
#4452=VERTEX_POINT('',#15091);
#4453=VERTEX_POINT('',#15093);
#4454=VERTEX_POINT('',#15097);
#4455=VERTEX_POINT('',#15099);
#4456=VERTEX_POINT('',#15103);
#4457=VERTEX_POINT('',#15105);
#4458=VERTEX_POINT('',#15113);
#4459=VERTEX_POINT('',#15116);
#4460=VERTEX_POINT('',#15120);
#4461=VERTEX_POINT('',#15124);
#5326=EDGE_CURVE('',#4446,#4447,#2757,.T.);
#5327=EDGE_CURVE('',#4446,#4448,#2758,.T.);
#5328=EDGE_CURVE('',#4448,#4449,#2759,.T.);
#5329=EDGE_CURVE('',#4447,#4449,#2760,.T.);
#5330=EDGE_CURVE('',#4450,#4446,#2761,.T.);
#5331=EDGE_CURVE('',#4450,#4451,#2762,.T.);
#5332=EDGE_CURVE('',#4451,#4448,#2763,.T.);
#5333=EDGE_CURVE('',#4452,#4450,#2764,.T.);
#5334=EDGE_CURVE('',#4452,#4453,#2765,.T.);
#5335=EDGE_CURVE('',#4453,#4451,#2766,.T.);
#5336=EDGE_CURVE('',#4454,#4452,#2767,.T.);
#5337=EDGE_CURVE('',#4454,#4455,#2768,.T.);
#5338=EDGE_CURVE('',#4455,#4453,#2769,.T.);
#5339=EDGE_CURVE('',#4456,#4454,#2770,.T.);
#5340=EDGE_CURVE('',#4456,#4457,#2771,.T.);
#5341=EDGE_CURVE('',#4457,#4455,#2772,.T.);
#5342=EDGE_CURVE('',#4447,#4456,#2773,.T.);
#5343=EDGE_CURVE('',#4449,#4457,#2774,.T.);
#5344=EDGE_CURVE('',#4458,#4458,#3864,.T.);
#5345=EDGE_CURVE('',#4459,#4459,#3865,.T.);
#5346=EDGE_CURVE('',#4459,#4458,#2775,.T.);
#5347=EDGE_CURVE('',#4460,#4460,#3866,.F.);
#5348=EDGE_CURVE('',#4460,#4459,#2776,.T.);
#5349=EDGE_CURVE('',#4461,#4461,#3867,.T.);
#5350=EDGE_CURVE('',#4461,#4460,#2777,.T.);
#6897=ORIENTED_EDGE('',*,*,#5326,.F.);
#6898=ORIENTED_EDGE('',*,*,#5327,.T.);
#6899=ORIENTED_EDGE('',*,*,#5328,.T.);
#6900=ORIENTED_EDGE('',*,*,#5329,.F.);
#6901=ORIENTED_EDGE('',*,*,#5330,.F.);
#6902=ORIENTED_EDGE('',*,*,#5331,.T.);
#6903=ORIENTED_EDGE('',*,*,#5332,.T.);
#6904=ORIENTED_EDGE('',*,*,#5327,.F.);
#6905=ORIENTED_EDGE('',*,*,#5333,.F.);
#6906=ORIENTED_EDGE('',*,*,#5334,.T.);
#6907=ORIENTED_EDGE('',*,*,#5335,.T.);
#6908=ORIENTED_EDGE('',*,*,#5331,.F.);
#6909=ORIENTED_EDGE('',*,*,#5336,.F.);
#6910=ORIENTED_EDGE('',*,*,#5337,.T.);
#6911=ORIENTED_EDGE('',*,*,#5338,.T.);
#6912=ORIENTED_EDGE('',*,*,#5334,.F.);
#6913=ORIENTED_EDGE('',*,*,#5339,.F.);
#6914=ORIENTED_EDGE('',*,*,#5340,.T.);
#6915=ORIENTED_EDGE('',*,*,#5341,.T.);
#6916=ORIENTED_EDGE('',*,*,#5337,.F.);
#6917=ORIENTED_EDGE('',*,*,#5342,.F.);
#6918=ORIENTED_EDGE('',*,*,#5329,.T.);
#6919=ORIENTED_EDGE('',*,*,#5343,.T.);
#6920=ORIENTED_EDGE('',*,*,#5340,.F.);
#6921=ORIENTED_EDGE('',*,*,#5343,.F.);
#6922=ORIENTED_EDGE('',*,*,#5328,.F.);
#6923=ORIENTED_EDGE('',*,*,#5332,.F.);
#6924=ORIENTED_EDGE('',*,*,#5335,.F.);
#6925=ORIENTED_EDGE('',*,*,#5338,.F.);
#6926=ORIENTED_EDGE('',*,*,#5341,.F.);
#6927=ORIENTED_EDGE('',*,*,#5344,.F.);
#6928=ORIENTED_EDGE('',*,*,#5326,.T.);
#6929=ORIENTED_EDGE('',*,*,#5342,.T.);
#6930=ORIENTED_EDGE('',*,*,#5339,.T.);
#6931=ORIENTED_EDGE('',*,*,#5336,.T.);
#6932=ORIENTED_EDGE('',*,*,#5333,.T.);
#6933=ORIENTED_EDGE('',*,*,#5330,.T.);
#6934=ORIENTED_EDGE('',*,*,#5345,.F.);
#6935=ORIENTED_EDGE('',*,*,#5346,.T.);
#6936=ORIENTED_EDGE('',*,*,#5344,.T.);
#6937=ORIENTED_EDGE('',*,*,#5346,.F.);
#6938=ORIENTED_EDGE('',*,*,#5347,.F.);
#6939=ORIENTED_EDGE('',*,*,#5348,.T.);
#6940=ORIENTED_EDGE('',*,*,#5345,.T.);
#6941=ORIENTED_EDGE('',*,*,#5348,.F.);
#6942=ORIENTED_EDGE('',*,*,#5349,.F.);
#6943=ORIENTED_EDGE('',*,*,#5350,.T.);
#6944=ORIENTED_EDGE('',*,*,#5347,.T.);
#6945=ORIENTED_EDGE('',*,*,#5350,.F.);
#6946=ORIENTED_EDGE('',*,*,#5349,.T.);
#8152=CYLINDRICAL_SURFACE('',#9942,0.1954);
#8490=ADVANCED_FACE('',(#1465),#1073,.F.);
#8491=ADVANCED_FACE('',(#1466),#1074,.F.);
#8492=ADVANCED_FACE('',(#1467),#1075,.F.);
#8493=ADVANCED_FACE('',(#1468),#1076,.F.);
#8494=ADVANCED_FACE('',(#1469),#1077,.F.);
#8495=ADVANCED_FACE('',(#1470),#1078,.F.);
#8496=ADVANCED_FACE('',(#1471),#1079,.F.);
#8497=ADVANCED_FACE('',(#1472,#822),#1080,.T.);
#8498=ADVANCED_FACE('',(#1473),#441,.T.);
#8499=ADVANCED_FACE('',(#1474),#8152,.T.);
#8500=ADVANCED_FACE('',(#1475),#442,.T.);
#8501=ADVANCED_FACE('',(#1476),#1081,.T.);
#8819=CLOSED_SHELL('',(#8490,#8491,#8492,#8493,#8494,#8495,#8496,#8497,
#8498,#8499,#8500,#8501));
#9930=AXIS2_PLACEMENT_3D('',#15074,#11807,#11808);
#9931=AXIS2_PLACEMENT_3D('',#15075,#11809,#11810);
#9932=AXIS2_PLACEMENT_3D('',#15084,#11815,#11816);
#9933=AXIS2_PLACEMENT_3D('',#15090,#11820,#11821);
#9934=AXIS2_PLACEMENT_3D('',#15096,#11825,#11826);
#9935=AXIS2_PLACEMENT_3D('',#15102,#11830,#11831);
#9936=AXIS2_PLACEMENT_3D('',#15108,#11835,#11836);
#9937=AXIS2_PLACEMENT_3D('',#15111,#11839,#11840);
#9938=AXIS2_PLACEMENT_3D('',#15112,#11841,#11842);
#9939=AXIS2_PLACEMENT_3D('',#15114,#11843,#11844);
#9940=AXIS2_PLACEMENT_3D('',#15115,#11845,#11846);
#9941=AXIS2_PLACEMENT_3D('',#15117,#11847,#11848);
#9942=AXIS2_PLACEMENT_3D('',#15119,#11850,#11851);
#9943=AXIS2_PLACEMENT_3D('',#15121,#11852,#11853);
#9944=AXIS2_PLACEMENT_3D('',#15123,#11855,#11856);
#9945=AXIS2_PLACEMENT_3D('',#15125,#11857,#11858);
#9946=AXIS2_PLACEMENT_3D('',#15127,#11860,#11861);
#11807=DIRECTION('axis',(0.,0.,1.));
#11808=DIRECTION('refdir',(1.,0.,0.));
#11809=DIRECTION('center_axis',(0.866025403784439,0.,-0.5));
#11810=DIRECTION('ref_axis',(0.5,0.,0.866025403784439));
#11811=DIRECTION('',(0.5,0.,0.866025403784439));
#11812=DIRECTION('',(0.,-1.,0.));
#11813=DIRECTION('',(0.5,0.,0.866025403784439));
#11814=DIRECTION('',(0.,-1.,0.));
#11815=DIRECTION('center_axis',(1.20185167898973E-16,0.,-1.));
#11816=DIRECTION('ref_axis',(1.,0.,1.20185167898973E-16));
#11817=DIRECTION('',(1.,0.,1.20185167898973E-16));
#11818=DIRECTION('',(0.,-1.,0.));
#11819=DIRECTION('',(1.,0.,1.20185167898973E-16));
#11820=DIRECTION('center_axis',(-0.866025403784439,0.,-0.5));
#11821=DIRECTION('ref_axis',(0.5,0.,-0.866025403784439));
#11822=DIRECTION('',(0.5,0.,-0.866025403784439));
#11823=DIRECTION('',(0.,-1.,0.));
#11824=DIRECTION('',(0.5,0.,-0.866025403784439));
#11825=DIRECTION('center_axis',(-0.866025403784439,0.,0.5));
#11826=DIRECTION('ref_axis',(-0.5,0.,-0.866025403784439));
#11827=DIRECTION('',(-0.5,0.,-0.866025403784439));
#11828=DIRECTION('',(0.,-1.,0.));
#11829=DIRECTION('',(-0.5,0.,-0.866025403784439));
#11830=DIRECTION('center_axis',(-2.40370335797945E-16,0.,1.));
#11831=DIRECTION('ref_axis',(-1.,0.,-2.40370335797945E-16));
#11832=DIRECTION('',(-1.,0.,-2.40370335797945E-16));
#11833=DIRECTION('',(0.,-1.,0.));
#11834=DIRECTION('',(-1.,0.,-2.40370335797945E-16));
#11835=DIRECTION('center_axis',(0.866025403784439,0.,0.5));
#11836=DIRECTION('ref_axis',(-0.5,0.,0.866025403784439));
#11837=DIRECTION('',(-0.5,0.,0.866025403784439));
#11838=DIRECTION('',(-0.5,0.,0.866025403784439));
#11839=DIRECTION('center_axis',(0.,-1.,0.));
#11840=DIRECTION('ref_axis',(0.,0.,-1.));
#11841=DIRECTION('center_axis',(0.,1.,0.));
#11842=DIRECTION('ref_axis',(0.,0.,1.));
#11843=DIRECTION('center_axis',(0.,-1.,0.));
#11844=DIRECTION('ref_axis',(1.,0.,0.));
#11845=DIRECTION('center_axis',(0.,-1.,0.));
#11846=DIRECTION('ref_axis',(1.,0.,0.));
#11847=DIRECTION('center_axis',(0.,-1.,0.));
#11848=DIRECTION('ref_axis',(1.,0.,0.));
#11849=DIRECTION('',(0.707106781186548,0.707106781186547,8.65956056235494E-17));
#11850=DIRECTION('center_axis',(0.,-1.,0.));
#11851=DIRECTION('ref_axis',(1.,0.,0.));
#11852=DIRECTION('center_axis',(0.,1.,0.));
#11853=DIRECTION('ref_axis',(1.,0.,0.));
#11854=DIRECTION('',(0.,1.,0.));
#11855=DIRECTION('center_axis',(0.,1.,0.));
#11856=DIRECTION('ref_axis',(1.,0.,0.));
#11857=DIRECTION('center_axis',(0.,-1.,0.));
#11858=DIRECTION('ref_axis',(1.,0.,0.));
#11859=DIRECTION('',(-0.707106781186548,0.707106781186547,-8.65956056235494E-17));
#11860=DIRECTION('center_axis',(0.,-1.,0.));
#11861=DIRECTION('ref_axis',(0.,0.,-1.));
#15074=CARTESIAN_POINT('',(0.,0.,0.));
#15075=CARTESIAN_POINT('Origin',(0.0577350269189626,0.,-0.1));
#15076=CARTESIAN_POINT('',(0.0577350269189626,0.,-0.1));
#15077=CARTESIAN_POINT('',(0.115470053837925,0.,0.));
#15078=CARTESIAN_POINT('',(0.0934187836487032,0.,-0.0381939203391614));
#15079=CARTESIAN_POINT('',(0.0577350269189626,-0.2,-0.1));
#15080=CARTESIAN_POINT('',(0.0577350269189626,0.,-0.1));
#15081=CARTESIAN_POINT('',(0.115470053837925,-0.2,0.));
#15082=CARTESIAN_POINT('',(0.115470053837925,-0.2,0.));
#15083=CARTESIAN_POINT('',(0.115470053837925,0.,0.));
#15084=CARTESIAN_POINT('Origin',(-0.0577350269189626,0.,-0.1));
#15085=CARTESIAN_POINT('',(-0.0577350269189626,0.,-0.1));
#15086=CARTESIAN_POINT('',(0.0561324865405187,0.,-0.1));
#15087=CARTESIAN_POINT('',(-0.0577350269189626,-0.2,-0.1));
#15088=CARTESIAN_POINT('',(-0.0577350269189626,0.,-0.1));
#15089=CARTESIAN_POINT('',(0.0577350269189626,-0.2,-0.1));
#15090=CARTESIAN_POINT('Origin',(-0.115470053837925,0.,-1.38777878078145E-17));
#15091=CARTESIAN_POINT('',(-0.115470053837925,0.,-1.41410031829988E-17));
#15092=CARTESIAN_POINT('',(-0.0797862971081845,0.,-0.0618060796608387));
#15093=CARTESIAN_POINT('',(-0.115470053837925,-0.2,-1.38777878078145E-17));
#15094=CARTESIAN_POINT('',(-0.115470053837925,0.,-1.41410031829988E-17));
#15095=CARTESIAN_POINT('',(-0.0577350269189626,-0.2,-0.1));
#15096=CARTESIAN_POINT('Origin',(-0.0577350269189626,0.,0.1));
#15097=CARTESIAN_POINT('',(-0.0577350269189626,0.,0.1));
#15098=CARTESIAN_POINT('',(-0.0509187836487033,0.,0.111806079660839));
#15099=CARTESIAN_POINT('',(-0.0577350269189626,-0.2,0.1));
#15100=CARTESIAN_POINT('',(-0.0577350269189626,0.,0.1));
#15101=CARTESIAN_POINT('',(-0.115470053837925,-0.2,-1.41410031829988E-17));
#15102=CARTESIAN_POINT('Origin',(0.0577350269189626,0.,0.1));
#15103=CARTESIAN_POINT('',(0.0577350269189626,0.,0.1));
#15104=CARTESIAN_POINT('',(0.113867513459481,0.,0.1));
#15105=CARTESIAN_POINT('',(0.0577350269189626,-0.2,0.1));
#15106=CARTESIAN_POINT('',(0.0577350269189626,0.,0.1));
#15107=CARTESIAN_POINT('',(-0.0577350269189626,-0.2,0.1));
#15108=CARTESIAN_POINT('Origin',(0.115470053837925,0.,0.));
#15109=CARTESIAN_POINT('',(0.122286297108185,0.,-0.0118060796608386));
#15110=CARTESIAN_POINT('',(0.0577350269189626,-0.2,0.1));
#15111=CARTESIAN_POINT('Origin',(0.,-0.2,0.));
#15112=CARTESIAN_POINT('Origin',(0.17,0.,0.));
#15113=CARTESIAN_POINT('',(-0.17,-8.67361737988404E-18,-2.0818995585505E-17));
#15114=CARTESIAN_POINT('Origin',(0.,0.,0.));
#15115=CARTESIAN_POINT('Origin',(0.,-0.015,0.));
#15116=CARTESIAN_POINT('',(-0.1954,-0.0254,-2.39295984553393E-17));
#15117=CARTESIAN_POINT('Origin',(0.,-0.0254,0.));
#15118=CARTESIAN_POINT('',(-0.185,-0.015,-2.2655965784226E-17));
#15119=CARTESIAN_POINT('Origin',(0.,-0.2775,0.));
#15120=CARTESIAN_POINT('',(-0.1954,-0.5296,2.39295984553393E-17));
#15121=CARTESIAN_POINT('Origin',(0.,-0.5296,0.));
#15122=CARTESIAN_POINT('',(-0.1954,-0.2775,-2.39295984553393E-17));
#15123=CARTESIAN_POINT('Origin',(0.,-0.5625,0.));
#15124=CARTESIAN_POINT('',(-0.125,-0.6,-1.53080849893419E-17));
#15125=CARTESIAN_POINT('Origin',(0.,-0.6,0.));
#15126=CARTESIAN_POINT('',(-0.1625,-0.5625,-1.99005104861445E-17));
#15127=CARTESIAN_POINT('Origin',(0.,-0.6,0.));
#16570=UNCERTAINTY_MEASURE_WITH_UNIT(LENGTH_MEASURE(0.001),#16679,
'DISTANCE_ACCURACY_VALUE',
'Maximum model space distance between geometric entities at asserted c
onnectivities');
#16614=UNCERTAINTY_MEASURE_WITH_UNIT(LENGTH_MEASURE(0.001),#16679,
'DISTANCE_ACCURACY_VALUE',
'Maximum model space distance between geometric entities at asserted c
onnectivities');
#16634=(
GEOMETRIC_REPRESENTATION_CONTEXT(3)
GLOBAL_UNCERTAINTY_ASSIGNED_CONTEXT((#16570))
GLOBAL_UNIT_ASSIGNED_CONTEXT((#16679,#16681,#16682))
REPRESENTATION_CONTEXT('','3D')
);
#16678=(
GEOMETRIC_REPRESENTATION_CONTEXT(3)
GLOBAL_UNCERTAINTY_ASSIGNED_CONTEXT((#16614))
GLOBAL_UNIT_ASSIGNED_CONTEXT((#16679,#16681,#16682))
REPRESENTATION_CONTEXT('','3D')
);
#16679=(
LENGTH_UNIT()
NAMED_UNIT(*)
SI_UNIT(.CENTI.,.METRE.)
);
#16681=(
NAMED_UNIT(*)
PLANE_ANGLE_UNIT()
SI_UNIT($,.RADIAN.)
);
#16682=(
NAMED_UNIT(*)
SI_UNIT($,.STERADIAN.)
SOLID_ANGLE_UNIT()
);
#16702=SHAPE_DEFINITION_REPRESENTATION(#16770,#16929);
#16770=PRODUCT_DEFINITION_SHAPE('',$,#16993);
#16929=SHAPE_REPRESENTATION('',(#9930),#16634);
#16973=PRODUCT_DEFINITION_CONTEXT('part definition',#17164,'design');
#16993=PRODUCT_DEFINITION('Socket Set Screw - M4x6',
'Socket Set Screw - M4x6',#17056,#16973);
#17056=PRODUCT_DEFINITION_FORMATION('',$,#17185);
#17164=APPLICATION_CONTEXT(
'Core Data for Automotive Mechanical Design Process');
#17165=PRODUCT_CONTEXT('part definition',#17164,'mechanical');
#17185=PRODUCT('Socket Set Screw - M4x6','Socket Set Screw - M4x6',
'Socket Set Screw - M4x6',(#17165));
#17292=COLOUR_RGB('Black',0.12,0.14,0.17);
#17293=FILL_AREA_STYLE_COLOUR('',#17292);
#17294=FILL_AREA_STYLE('',(#17293));
#17295=SURFACE_STYLE_FILL_AREA(#17294);
#17296=SURFACE_SIDE_STYLE('',(#17295));
#17297=SURFACE_STYLE_USAGE(.BOTH.,#17296);
#17298=PRESENTATION_STYLE_ASSIGNMENT((#17297));
ENDSEC;
END-ISO-10303-21;
